ISO-10303-21;
HEADER;
/* Generated by software containing ST-Developer
 * from STEP Tools, Inc. (www.steptools.com) 
 */

FILE_DESCRIPTION(
/* description */ ('Guided pneumatic stop gate'),
/* implementation_level */ '2;1');

FILE_NAME(
/* name */ 'Flat Washer - M6 (1).step',
/* time_stamp */ '2026-10-27T21:43:45-07:00',
/* author */ (''),
/* organization */ (''),
/* preprocessor_version */ 'ST-DEVELOPER v20.2',
/* originating_system */ 'Autodesk Translation Framework v15.17.0.0',
/* authorisation */ '');

FILE_SCHEMA (('AUTOMOTIVE_DESIGN { 1 0 10303 214 3 1 1 }'));
ENDSEC;

DATA;
#10=MECHANICAL_DESIGN_GEOMETRIC_PRESENTATION_REPRESENTATION('',(#575),#14392);
#491=SHAPE_REPRESENTATION_RELATIONSHIP('SRR','None',#14628,#533);
#533=ADVANCED_BREP_SHAPE_REPRESENTATION('',(#613),#14390);
#575=STYLED_ITEM('',(#14898),#613);
#613=MANIFOLD_SOLID_BREP('Body1',#7919);
#821=FACE_BOUND('',#2262,.T.);
#822=FACE_BOUND('',#2264,.T.);
#1108=PLANE('',#9343);
#1109=PLANE('',#9344);
#1578=FACE_OUTER_BOUND('',#2259,.T.);
#1579=FACE_OUTER_BOUND('',#2260,.T.);
#1580=FACE_OUTER_BOUND('',#2261,.T.);
#1581=FACE_OUTER_BOUND('',#2263,.T.);
#2259=EDGE_LOOP('',(#7174,#7175,#7176,#7177));
#2260=EDGE_LOOP('',(#7178,#7179,#7180,#7181));
#2261=EDGE_LOOP('',(#7182));
#2262=EDGE_LOOP('',(#7183));
#2263=EDGE_LOOP('',(#7184));
#2264=EDGE_LOOP('',(#7185));
#2812=LINE('',#14190,#3357);
#2813=LINE('',#14196,#3358);
#3357=VECTOR('',#11825,0.32);
#3358=VECTOR('',#11832,0.6);
#3729=CIRCLE('',#9338,0.32);
#3730=CIRCLE('',#9339,0.32);
#3731=CIRCLE('',#9341,0.6);
#3732=CIRCLE('',#9342,0.6);
#4336=VERTEX_POINT('',#14187);
#4337=VERTEX_POINT('',#14189);
#4338=VERTEX_POINT('',#14193);
#4339=VERTEX_POINT('',#14195);
#5285=EDGE_CURVE('',#4336,#4336,#3729,.T.);
#5286=EDGE_CURVE('',#4336,#4337,#2812,.T.);
#5287=EDGE_CURVE('',#4337,#4337,#3730,.T.);
#5288=EDGE_CURVE('',#4338,#4338,#3731,.T.);
#5289=EDGE_CURVE('',#4338,#4339,#2813,.T.);
#5290=EDGE_CURVE('',#4339,#4339,#3732,.T.);
#7174=ORIENTED_EDGE('',*,*,#5285,.F.);
#7175=ORIENTED_EDGE('',*,*,#5286,.T.);
#7176=ORIENTED_EDGE('',*,*,#5287,.T.);
#7177=ORIENTED_EDGE('',*,*,#5286,.F.);
#7178=ORIENTED_EDGE('',*,*,#5288,.F.);
#7179=ORIENTED_EDGE('',*,*,#5289,.T.);
#7180=ORIENTED_EDGE('',*,*,#5290,.T.);
#7181=ORIENTED_EDGE('',*,*,#5289,.F.);
#7182=ORIENTED_EDGE('',*,*,#5288,.T.);
#7183=ORIENTED_EDGE('',*,*,#5285,.T.);
#7184=ORIENTED_EDGE('',*,*,#5290,.F.);
#7185=ORIENTED_EDGE('',*,*,#5287,.F.);
#7397=CYLINDRICAL_SURFACE('',#9337,0.32);
#7398=CYLINDRICAL_SURFACE('',#9340,0.6);
#7860=ADVANCED_FACE('',(#1578),#7397,.F.);
#7861=ADVANCED_FACE('',(#1579),#7398,.T.);
#7862=ADVANCED_FACE('',(#1580,#821),#1108,.T.);
#7863=ADVANCED_FACE('',(#1581,#822),#1109,.F.);
#7919=CLOSED_SHELL('',(#7860,#7861,#7862,#7863));
#9336=AXIS2_PLACEMENT_3D('',#14185,#11819,#11820);
#9337=AXIS2_PLACEMENT_3D('',#14186,#11821,#11822);
#9338=AXIS2_PLACEMENT_3D('',#14188,#11823,#11824);
#9339=AXIS2_PLACEMENT_3D('',#14191,#11826,#11827);
#9340=AXIS2_PLACEMENT_3D('',#14192,#11828,#11829);
#9341=AXIS2_PLACEMENT_3D('',#14194,#11830,#11831);
#9342=AXIS2_PLACEMENT_3D('',#14197,#11833,#11834);
#9343=AXIS2_PLACEMENT_3D('',#14198,#11835,#11836);
#9344=AXIS2_PLACEMENT_3D('',#14199,#11837,#11838);
#11819=DIRECTION('axis',(0.,0.,1.));
#11820=DIRECTION('refdir',(1.,0.,0.));
#11821=DIRECTION('center_axis',(0.,1.,0.));
#11822=DIRECTION('ref_axis',(1.,0.,0.));
#11823=DIRECTION('center_axis',(0.,-1.,0.));
#11824=DIRECTION('ref_axis',(1.,0.,0.));
#11825=DIRECTION('',(0.,-1.,0.));
#11826=DIRECTION('center_axis',(0.,-1.,0.));
#11827=DIRECTION('ref_axis',(1.,0.,0.));
#11828=DIRECTION('center_axis',(0.,1.,0.));
#11829=DIRECTION('ref_axis',(1.,0.,0.));
#11830=DIRECTION('center_axis',(0.,1.,0.));
#11831=DIRECTION('ref_axis',(1.,0.,0.));
#11832=DIRECTION('',(0.,-1.,0.));
#11833=DIRECTION('center_axis',(0.,1.,0.));
#11834=DIRECTION('ref_axis',(1.,0.,0.));
#11835=DIRECTION('center_axis',(0.,1.,0.));
#11836=DIRECTION('ref_axis',(1.,0.,0.));
#11837=DIRECTION('center_axis',(0.,1.,0.));
#11838=DIRECTION('ref_axis',(1.,0.,0.));
#14185=CARTESIAN_POINT('',(0.,0.,0.));
#14186=CARTESIAN_POINT('Origin',(0.,0.,0.));
#14187=CARTESIAN_POINT('',(-0.32,0.16,3.91886975727153E-17));
#14188=CARTESIAN_POINT('Origin',(0.,0.16,0.));
#14189=CARTESIAN_POINT('',(-0.32,0.,3.91886975727153E-17));
#14190=CARTESIAN_POINT('',(-0.32,0.,3.91886975727153E-17));
#14191=CARTESIAN_POINT('Origin',(0.,0.,0.));
#14192=CARTESIAN_POINT('Origin',(0.,0.,0.));
#14193=CARTESIAN_POINT('',(-0.6,0.16,7.34788079488412E-17));
#14194=CARTESIAN_POINT('Origin',(0.,0.16,0.));
#14195=CARTESIAN_POINT('',(-0.6,0.,7.34788079488412E-17));
#14196=CARTESIAN_POINT('',(-0.6,0.,7.34788079488412E-17));
#14197=CARTESIAN_POINT('Origin',(0.,0.,0.));
#14198=CARTESIAN_POINT('Origin',(0.,0.16,0.));
#14199=CARTESIAN_POINT('Origin',(0.,0.,0.));
#14342=UNCERTAINTY_MEASURE_WITH_UNIT(LENGTH_MEASURE(0.001),#14393,
'DISTANCE_ACCURACY_VALUE',
'Maximum model space distance between geometric entities at asserted c
onnectivities');
#14344=UNCERTAINTY_MEASURE_WITH_UNIT(LENGTH_MEASURE(0.001),#14393,
'DISTANCE_ACCURACY_VALUE',
'Maximum model space distance between geometric entities at asserted c
onnectivities');
#14390=(
GEOMETRIC_REPRESENTATION_CONTEXT(3)
GLOBAL_UNCERTAINTY_ASSIGNED_CONTEXT((#14342))
GLOBAL_UNIT_ASSIGNED_CONTEXT((#14393,#14395,#14396))
REPRESENTATION_CONTEXT('','3D')
);
#14392=(
GEOMETRIC_REPRESENTATION_CONTEXT(3)
GLOBAL_UNCERTAINTY_ASSIGNED_CONTEXT((#14344))
GLOBAL_UNIT_ASSIGNED_CONTEXT((#14393,#14395,#14396))
REPRESENTATION_CONTEXT('','3D')
);
#14393=(
LENGTH_UNIT()
NAMED_UNIT(*)
SI_UNIT(.CENTI.,.METRE.)
);
#14395=(
NAMED_UNIT(*)
PLANE_ANGLE_UNIT()
SI_UNIT($,.RADIAN.)
);
#14396=(
NAMED_UNIT(*)
SI_UNIT($,.STERADIAN.)
SOLID_ANGLE_UNIT()
);
#14442=SHAPE_DEFINITION_REPRESENTATION(#14561,#14628);
#14561=PRODUCT_DEFINITION_SHAPE('',$,#14676);
#14628=SHAPE_REPRESENTATION('',(#9336),#14390);
#14630=PRODUCT_DEFINITION_CONTEXT('part definition',#14773,'design');
#14676=PRODUCT_DEFINITION('Flat Washer - M6 (1)','Flat Washer - M6 (1)',#14723,
#14630);
#14723=PRODUCT_DEFINITION_FORMATION('',$,#14820);
#14773=APPLICATION_CONTEXT(
'Core Data for Automotive Mechanical Design Process');
#14774=PRODUCT_CONTEXT('part definition',#14773,'mechanical');
#14820=PRODUCT('Flat Washer - M6 (1)','Flat Washer - M6 (1)',
'Flat Washer - M6 (1)',(#14774));
#14892=COLOUR_RGB('Black',0.12,0.14,0.17);
#14893=FILL_AREA_STYLE_COLOUR('',#14892);
#14894=FILL_AREA_STYLE('',(#14893));
#14895=SURFACE_STYLE_FILL_AREA(#14894);
#14896=SURFACE_SIDE_STYLE('',(#14895));
#14897=SURFACE_STYLE_USAGE(.BOTH.,#14896);
#14898=PRESENTATION_STYLE_ASSIGNMENT((#14897));
ENDSEC;
END-ISO-10303-21;
